ISO-10303-21;
HEADER;
FILE_DESCRIPTION (('STEP AP203'),
    '1' );
FILE_NAME ('Pin 2.step',
    '2026-10-31T14:11:27',
    ( '' ),
    ( '' ),
    'SwSTEP 2.0',
    'SolidWorks 2024',
    '' );
FILE_SCHEMA (( 'AUTOMOTIVE_DESIGN' ));
ENDSEC;

DATA;
#11=CARTESIAN_POINT ( 'NONE',  ( 34.15720538308221421, 9.344634530308759679, 27.44000000000022865 ) ) ;
#14=DIRECTION ( 'NONE',  ( -0.2306359803922088947, -0.9730401042858021210, 5.139921410301650007E-15 ) ) ;
#27=FACE_OUTER_BOUND ( 'NONE', #19207, .T. ) ;
#53=CARTESIAN_POINT ( 'NONE',  ( 37.91003399039540511, 9.225896048120093340, 26.88000000000000611 ) ) ;
#112=ORIENTED_EDGE ( 'NONE', *, *, #10125, .F. ) ;
#151=PLANE ( 'NONE',  #7708 ) ;
#315=ORIENTED_EDGE ( 'NONE', *, *, #19389, .F. ) ;
#322=CIRCLE ( 'NONE', #3373, 2.369999999999999218 ) ;
#363=CIRCLE ( 'NONE', #383, 2.700000000000000178 ) ;
#383=AXIS2_PLACEMENT_3D ( 'NONE', #981, #4553, #22949 ) ;
#415=DIRECTION ( 'NONE',  ( 1.000000000000000000, 0.000000000000000000, 0.000000000000000000 ) ) ;
#437=ORIENTED_EDGE ( 'NONE', *, *, #10962, .F. ) ;
#444=VECTOR ( 'NONE', #7289, 1000.000000000000000 ) ;
#469=ORIENTED_EDGE ( 'NONE', *, *, #21827, .F. ) ;
#515=FACE_OUTER_BOUND ( 'NONE', #10689, .T. ) ;
#766=LINE ( 'NONE', #17049, #8494 ) ;
#779=CARTESIAN_POINT ( 'NONE',  ( 36.17078849317573486, 12.20740994216804154, 26.29999999999999005 ) ) ;
#981=CARTESIAN_POINT ( 'NONE',  ( 35.59419854219520118, 9.774809681453540122, 26.50000000000000000 ) ) ;
#989=VERTEX_POINT ( 'NONE', #6967 ) ;
#998=VECTOR ( 'NONE', #17041, 1000.000000000000000 ) ;
#1065=CARTESIAN_POINT ( 'NONE',  ( 35.59419854219520118, 9.774809681453469068, 10.50000000000020073 ) ) ;
#1127=EDGE_CURVE ( 'NONE', #13630, #15927, #19891, .T. ) ;
#1129=ORIENTED_EDGE ( 'NONE', *, *, #17707, .F. ) ;
#1173=DIRECTION ( 'NONE',  ( -0.9579954394086687142, -0.2867834340965179640, 1.451283422213139767E-15 ) ) ;
#1189=DIRECTION ( 'NONE',  ( 6.123230199561429643E-17, 4.868008300101910084E-15, 1.000000000000000000 ) ) ;
#1264=ORIENTED_EDGE ( 'NONE', *, *, #2892, .F. ) ;
#1315=ORIENTED_EDGE ( 'NONE', *, *, #5444, .F. ) ;
#1354=EDGE_CURVE ( 'NONE', #15994, #8200, #9793, .T. ) ;
#1429=CIRCLE ( 'NONE', #12082, 2.500000000000000888 ) ;
#1452=CARTESIAN_POINT ( 'NONE',  ( 34.40556712239430226, 8.514986143071229918, 27.68999999999999773 ) ) ;
#1477=ORIENTED_EDGE ( 'NONE', *, *, #11222, .T. ) ;
#1535=DIRECTION ( 'NONE',  ( 6.123230199561449365E-17, 4.868008300101910084E-15, 1.000000000000000000 ) ) ;
#1635=CARTESIAN_POINT ( 'NONE',  ( 35.59419854219520118, 9.774809681453540122, 26.50000000000000000 ) ) ;
#1692=DIRECTION ( 'NONE',  ( -5.964507377817269296E-17, -4.861311874385510251E-15, -1.000000000000000000 ) ) ;
#1704=ADVANCED_BREP_SHAPE_REPRESENTATION ( '', ( #16939, #12739 ), #21233 ) ;
#1706=ORIENTED_EDGE ( 'NONE', *, *, #22263, .T. ) ;
#1712=EDGE_CURVE ( 'NONE', #7633, #13130, #7990, .T. ) ;
#1800=DIRECTION ( 'NONE',  ( -0.2306359803922101992, -0.9730401042858018990, 4.616450158279816491E-15 ) ) ;
#1850=PLANE ( 'NONE',  #23330 ) ;
#1870=ORIENTED_EDGE ( 'NONE', *, *, #17946, .T. ) ;
#1899=VERTEX_POINT ( 'NONE', #2745 ) ;
#1908=CARTESIAN_POINT ( 'NONE',  ( 35.59419854219520118, 9.774809681453469068, 10.50000000000020073 ) ) ;
#1920=CARTESIAN_POINT ( 'NONE',  ( 35.59419854219520118, 9.774809681453540122, 26.30000000000000071 ) ) ;
#1931=DIRECTION ( 'NONE',  ( 3.764133351409869857E-47, -1.000000000000000000, 4.861311874385510251E-15 ) ) ;
#2025=DIRECTION ( 'NONE',  ( 6.123230199561429643E-17, 4.868008300101910084E-15, 1.000000000000000000 ) ) ;
#2051=CARTESIAN_POINT ( 'NONE',  ( 37.27955344062029752, 9.375336445360789028, 29.25000000000000000 ) ) ;
#2125=DIRECTION ( 'NONE',  ( -4.526956032885830318E-15, -4.330888464475804873E-31, 1.000000000000000000 ) ) ;
#2126=ORIENTED_EDGE ( 'NONE', *, *, #13290, .F. ) ;
#2128=CARTESIAN_POINT ( 'NONE',  ( 35.59419854219520118, 9.774809681453550780, 26.88000000000000256 ) ) ;
#2145=DIRECTION ( 'NONE',  ( -0.2306359803922101437, -0.9730401042858017879, 4.316864774682981680E-15 ) ) ;
#2154=AXIS2_PLACEMENT_3D ( 'NONE', #1920, #7408, #9179 ) ;
#2157=CARTESIAN_POINT ( 'NONE',  ( 36.11419503630708050, 11.96864536137832324, 10.74538000000018911 ) ) ;
#2166=ORIENTED_EDGE ( 'NONE', *, *, #11222, .F. ) ;
#2213=CARTESIAN_POINT ( 'NONE',  ( 38.02679880290970260, 9.198219730473017108, 26.30000000000000426 ) ) ;
#2239=FACE_OUTER_BOUND ( 'NONE', #13971, .T. ) ;
#2317=FACE_OUTER_BOUND ( 'NONE', #17838, .T. ) ;
#2382=ORIENTED_EDGE ( 'NONE', *, *, #21827, .T. ) ;
#2465=ORIENTED_EDGE ( 'NONE', *, *, #11732, .F. ) ;
#2473=ORIENTED_EDGE ( 'NONE', *, *, #13290, .T. ) ;
#2496=ORIENTED_EDGE ( 'NONE', *, *, #4549, .T. ) ;
#2513=ORIENTED_EDGE ( 'NONE', *, *, #17946, .F. ) ;
#2518=EDGE_CURVE ( 'NONE', #12383, #14944, #18829, .T. ) ;
#2544=AXIS2_PLACEMENT_3D ( 'NONE', #13583, #20824, #4554 ) ;
#2564=AXIS2_PLACEMENT_3D ( 'NONE', #14489, #1535, #12376 ) ;
#2569=CARTESIAN_POINT ( 'NONE',  ( 0.000000000000000000, 0.000000000000000000, 0.000000000000000000 ) ) ;
#2620=VERTEX_POINT ( 'NONE', #6707 ) ;
#2637=ORIENTED_EDGE ( 'NONE', *, *, #5444, .T. ) ;
#2668=DIRECTION ( 'NONE',  ( 7.252994924361790472E-16, -5.047364287626240282E-15, -1.000000000000000000 ) ) ;
#2670=VECTOR ( 'NONE', #16410, 1000.000000000000000 ) ;
#2696=LINE ( 'NONE', #6496, #16825 ) ;
#2745=CARTESIAN_POINT ( 'NONE',  ( 36.78282996199610722, 11.03463321983590006, 27.68999999999999773 ) ) ;
#2825=ORIENTED_EDGE ( 'NONE', *, *, #17900, .T. ) ;
#2826=AXIS2_PLACEMENT_3D ( 'NONE', #1635, #23253, #19580 ) ;
#2834=FACE_OUTER_BOUND ( 'NONE', #6498, .T. ) ;
#2844=VERTEX_POINT ( 'NONE', #12401 ) ;
#2849=LINE ( 'NONE', #19133, #5429 ) ;
#2892=EDGE_CURVE ( 'NONE', #10793, #15994, #7172, .T. ) ;
#2905=ORIENTED_EDGE ( 'NONE', *, *, #18238, .F. ) ;
#2956=DIRECTION ( 'NONE',  ( 0.1997366180463827634, 0.8426774492125668203, 0.4999999999999953371 ) ) ;
#3000=EDGE_CURVE ( 'NONE', #7633, #18172, #9992, .T. ) ;
#3025=LINE ( 'NONE', #17170, #998 ) ;
#3047=AXIS2_PLACEMENT_3D ( 'NONE', #1908, #18554, #2145 ) ;
#3074=DIRECTION ( 'NONE',  ( 6.052506032659479608E-17, 4.865024487662030352E-15, 1.000000000000000000 ) ) ;
#3133=DIRECTION ( 'NONE',  ( 7.252994924361790472E-16, -5.047364287626240282E-15, -1.000000000000000000 ) ) ;
#3190=ORIENTED_EDGE ( 'NONE', *, *, #10159, .T. ) ;
#3268=CARTESIAN_POINT ( 'NONE',  ( 35.09747506357100377, 11.43410645592859964, 27.68999999999999773 ) ) ;
#3359=FACE_OUTER_BOUND ( 'NONE', #10493, .T. ) ;
#3373=AXIS2_PLACEMENT_3D ( 'NONE', #53, #7328, #18244 ) ;
#3393=VERTEX_POINT ( 'NONE', #16579 ) ;
#3442=ORIENTED_EDGE ( 'NONE', *, *, #22183, .F. ) ;
#3474=LINE ( 'NONE', #11090, #2670 ) ;
#3535=AXIS2_PLACEMENT_3D ( 'NONE', #19886, #21525, #3716 ) ;
#3567=( NAMED_UNIT ( * ) PLANE_ANGLE_UNIT ( ) SI_UNIT ( $, .RADIAN. ) );
#3599=CARTESIAN_POINT ( 'NONE',  ( 35.59419854219520118, 9.774809681453469068, 10.74538000000019977 ) ) ;
#3603=CARTESIAN_POINT ( 'NONE',  ( 36.78282996199610722, 11.03463321983590006, 28.46999999999999886 ) ) ;
#3614=CARTESIAN_POINT ( 'NONE',  ( 36.68971944905818816, 14.39675017681111058, 27.87499999999997513 ) ) ;
#3691=AXIS2_PLACEMENT_3D ( 'NONE', #12605, #16038, #19601 ) ;
#3716=DIRECTION ( 'NONE',  ( 0.2306359803922102825, 0.9730401042858017879, -4.163336342344335449E-15 ) ) ;
#3720=EDGE_CURVE ( 'NONE', #10793, #989, #6541, .T. ) ;
#3752=CARTESIAN_POINT ( 'NONE',  ( 33.16159828148069266, 10.35139963243406314, 26.29999999999999716 ) ) ;
#3784=ORIENTED_EDGE ( 'NONE', *, *, #4549, .F. ) ;
#3889=EDGE_LOOP ( 'NONE', ( #16454, #2382, #6661, #12524, #12318 ) ) ;
#3953=CIRCLE ( 'NONE', #2826, 4.750000000000000000 ) ;
#4016=ORIENTED_EDGE ( 'NONE', *, *, #22281, .F. ) ;
#4047=ADVANCED_FACE ( 'NONE', ( #11720 ), #20479, .F. ) ;
#4068=SHAPE_DEFINITION_REPRESENTATION ( #16116, #7508 ) ;
#4120=CARTESIAN_POINT ( 'NONE',  ( 35.59419854219520118, 9.774809681453540122, 26.30000000000000071 ) ) ;
#4237=CARTESIAN_POINT ( 'NONE',  ( 36.09092202081949807, 8.115512906978459284, 27.68999999999999773 ) ) ;
#4298=CIRCLE ( 'NONE', #4315, 4.750000000000000000 ) ;
#4315=AXIS2_PLACEMENT_3D ( 'NONE', #20247, #7537, #18713 ) ;
#4367=EDGE_LOOP ( 'NONE', ( #16638, #15678, #11628, #12234 ) ) ;
#4376=ORIENTED_EDGE ( 'NONE', *, *, #13043, .T. ) ;
#4476=CARTESIAN_POINT ( 'NONE',  ( 37.27955344062029752, 9.375336445360778370, 27.68999999999999773 ) ) ;
#4494=FACE_BOUND ( 'NONE', #10057, .T. ) ;
#4549=EDGE_CURVE ( 'NONE', #8090, #2844, #9783, .T. ) ;
#4553=DIRECTION ( 'NONE',  ( -5.964507377817318600E-17, -4.861311874385510251E-15, -1.000000000000000000 ) ) ;
#4554=DIRECTION ( 'NONE',  ( -0.2306359803922084506, -0.9730401042858020100, 5.112869192352694760E-15 ) ) ;
#4591=DIRECTION ( 'NONE',  ( 6.123230199561459225E-17, 4.868008300101910084E-15, 1.000000000000000000 ) ) ;
#4615=DIRECTION ( 'NONE',  ( 2.899533054064307511E-31, 4.861311874385510251E-15, 1.000000000000000000 ) ) ;
#4626=CARTESIAN_POINT ( 'NONE',  ( 35.79393516024158117, 10.61748713066611494, 27.18999999999999417 ) ) ;
#4705=DIRECTION ( 'NONE',  ( -0.2306359803922090335, -0.9730401042858022320, 4.744007713284279563E-15 ) ) ;
#4913=CARTESIAN_POINT ( 'NONE',  ( 35.59419854219520118, 9.774809681453550780, 26.88000000000000256 ) ) ;
#5057=DIRECTION ( 'NONE',  ( -5.964507377817349415E-17, -4.861311874385510251E-15, -1.000000000000000000 ) ) ;
#5067=CARTESIAN_POINT ( 'NONE',  ( 36.68971944905818816, 14.39675017681111058, 26.87999999999997769 ) ) ;
#5074=CARTESIAN_POINT ( 'NONE',  ( 34.85715660638717139, 8.407947612062324438, 27.55602540378454535 ) ) ;
#5075=ORIENTED_EDGE ( 'NONE', *, *, #12480, .F. ) ;
#5102=DIRECTION ( 'NONE',  ( -0.2306359803922101992, -0.9730401042858018990, 4.616450158279816491E-15 ) ) ;
#5118=EDGE_LOOP ( 'NONE', ( #13686, #437 ) ) ;
#5176=EDGE_LOOP ( 'NONE', ( #13243, #16470 ) ) ;
#5192=EDGE_CURVE ( 'NONE', #13418, #21387, #6443, .T. ) ;
#5228=VECTOR ( 'NONE', #12942, 999.9999999999998863 ) ;
#5268=ORIENTED_EDGE ( 'NONE', *, *, #18337, .F. ) ;
#5328=AXIS2_PLACEMENT_3D ( 'NONE', #11928, #15565, #22802 ) ;
#5429=VECTOR ( 'NONE', #6406, 999.9999999999998863 ) ;
#5444=EDGE_CURVE ( 'NONE', #20801, #16051, #322, .T. ) ;
#5450=EDGE_LOOP ( 'NONE', ( #8169, #6274 ) ) ;
#5496=ADVANCED_FACE ( 'NONE', ( #2317 ), #6038, .T. ) ;
#5602=CARTESIAN_POINT ( 'NONE',  ( 35.59419854219520118, 9.774809681453469068, 10.99076000000020059 ) ) ;
#5677=AXIS2_PLACEMENT_3D ( 'NONE', #4913, #3133, #8715 ) ;
#5686=CARTESIAN_POINT ( 'NONE',  ( 34.80031720862070443, 11.11915057133309936, 29.25000000000000000 ) ) ;
#5687=DIRECTION ( 'NONE',  ( -0.2306359803922084506, -0.9730401042858020100, 5.112869192352694760E-15 ) ) ;
#5720=CARTESIAN_POINT ( 'NONE',  ( 37.27955344062029752, 9.375336445360789028, 28.46999999999999886 ) ) ;
#5930=DIRECTION ( 'NONE',  ( -0.7273594590164595974, 0.6862566701892837129, -3.292724291071135063E-15 ) ) ;
#6000=AXIS2_PLACEMENT_3D ( 'NONE', #19054, #13698, #15719 ) ;
#6038=TOROIDAL_SURFACE ( 'NONE', #19741, 2.380000000000000338, 2.370000000000000107 ) ;
#6076=DIRECTION ( 'NONE',  ( 0.2306359803922084506, 0.9730401042858022320, -5.112869192352694760E-15 ) ) ;
#6115=( BOUNDED_CURVE ( )  B_SPLINE_CURVE ( 2, ( #22025, #11259, #14441 ),
 .UNSPECIFIED., .F., .F. ) 
 B_SPLINE_CURVE_WITH_KNOTS ( ( 3, 3 ),
 ( 0.000000000000000000, 0.08763271035584448143 ),
 .UNSPECIFIED. ) 
 CURVE ( )  GEOMETRIC_REPRESENTATION_ITEM ( )  RATIONAL_B_SPLINE_CURVE ( ( 1.000000000000000000, 1.077350269189626175, 1.077350269189624843 ) ) 
 REPRESENTATION_ITEM ( '' )  );
#6119=ORIENTED_EDGE ( 'NONE', *, *, #8601, .T. ) ;
#6132=DIRECTION ( 'NONE',  ( -6.123230199561449365E-17, -4.868008300101910084E-15, -1.000000000000000000 ) ) ;
#6149=EDGE_LOOP ( 'NONE', ( #12835, #9190, #2126, #22120 ) ) ;
#6274=ORIENTED_EDGE ( 'NONE', *, *, #22263, .F. ) ;
#6340=AXIS2_PLACEMENT_3D ( 'NONE', #3599, #10869, #1800 ) ;
#6369=CARTESIAN_POINT ( 'NONE',  ( 37.27955344062029752, 9.375336445360778370, 27.68999999999999773 ) ) ;
#6393=CARTESIAN_POINT ( 'NONE',  ( 35.94015251278350576, 11.23436983788223209, 27.55602540378454179 ) ) ;
#6406=DIRECTION ( 'NONE',  ( -0.6862566701892842680, -0.7273594590164591533, 3.576853004787541598E-15 ) ) ;
#6426=DIRECTION ( 'NONE',  ( 5.964507377817298878E-17, 4.861311874385510251E-15, 1.000000000000000000 ) ) ;
#6443=CIRCLE ( 'NONE', #20478, 0.2000000000000016209 ) ;
#6496=CARTESIAN_POINT ( 'NONE',  ( 34.82690584700060299, 8.415117834048050582, 29.25000000000000000 ) ) ;
#6498=EDGE_LOOP ( 'NONE', ( #20289, #6653, #5268, #315, #4016 ) ) ;
#6516=MECHANICAL_CONTEXT ( 'NONE', #17171, 'mechanical' ) ;
#6541=( BOUNDED_CURVE ( )  B_SPLINE_CURVE ( 2, ( #13741, #5074, #23220 ),
 .UNSPECIFIED., .F., .F. ) 
 B_SPLINE_CURVE_WITH_KNOTS ( ( 3, 3 ),
 ( 0.000000000000000000, 0.08763271035584378754 ),
 .UNSPECIFIED. ) 
 CURVE ( )  GEOMETRIC_REPRESENTATION_ITEM ( )  RATIONAL_B_SPLINE_CURVE ( ( 1.000000000000000000, 1.077350269189625731, 1.077350269189625065 ) ) 
 REPRESENTATION_ITEM ( '' )  );
#6623=DESIGN_CONTEXT ( 'detailed design', #14278, 'design' ) ;
#6653=ORIENTED_EDGE ( 'NONE', *, *, #2892, .T. ) ;
#6661=ORIENTED_EDGE ( 'NONE', *, *, #10889, .T. ) ;
#6707=CARTESIAN_POINT ( 'NONE',  ( 36.09092202081949807, 8.115512906978469942, 29.25000000000000000 ) ) ;
#6723=CARTESIAN_POINT ( 'NONE',  ( 35.54906454756380185, 11.32706792491969772, 27.55602540378455600 ) ) ;
#6737=VERTEX_POINT ( 'NONE', #19012 ) ;
#6769=ADVANCED_FACE ( 'NONE', ( #13657 ), #12020, .F. ) ;
#6967=CARTESIAN_POINT ( 'NONE',  ( 35.24824457160688240, 8.315249525024842825, 27.55602540378454535 ) ) ;
#6999=EDGE_CURVE ( 'NONE', #12383, #8090, #7469, .T. ) ;
#7001=AXIS2_PLACEMENT_3D ( 'NONE', #2128, #2025, #5687 ) ;
#7030=ORIENTED_EDGE ( 'NONE', *, *, #22108, .F. ) ;
#7144=CARTESIAN_POINT ( 'NONE',  ( 33.90884364377009774, 10.17428291754630010, 27.68999999999999773 ) ) ;
#7147=CARTESIAN_POINT ( 'NONE',  ( 35.01760859121468883, 7.342209420739032488, 26.30000000000001137 ) ) ;
#7172=LINE ( 'NONE', #21518, #15801 ) ;
#7182=EDGE_CURVE ( 'NONE', #23367, #16446, #8074, .T. ) ;
#7242=CIRCLE ( 'NONE', #5328, 2.369999999999999218 ) ;
#7261=CARTESIAN_POINT ( 'NONE',  ( 32.96699026062353255, 10.39752682851250576, 26.49999999999999645 ) ) ;
#7262=EDGE_LOOP ( 'NONE', ( #15460, #12068, #16306, #4376 ) ) ;
#7289=DIRECTION ( 'NONE',  ( 5.964507377817269296E-17, 4.861311874385510251E-15, 1.000000000000000000 ) ) ;
#7328=DIRECTION ( 'NONE',  ( 0.2306359803922089224, 0.9730401042858022320, -4.744007713284281141E-15 ) ) ;
#7348=ORIENTED_EDGE ( 'NONE', *, *, #18238, .T. ) ;
#7408=DIRECTION ( 'NONE',  ( 6.123230199561459225E-17, 4.868008300101910084E-15, 1.000000000000000000 ) ) ;
#7418=CARTESIAN_POINT ( 'NONE',  ( 36.43025397111700414, 13.30208005948959915, 26.50000000000000000 ) ) ;
#7469=LINE ( 'NONE', #19823, #18718 ) ;
#7474=CIRCLE ( 'NONE', #15432, 2.700000000000000178 ) ;
#7508=SHAPE_REPRESENTATION ( 'Pin 2', ( #12739 ), #21233 ) ;
#7511=EDGE_CURVE ( 'NONE', #16051, #13630, #4298, .T. ) ;
#7525=UNCERTAINTY_MEASURE_WITH_UNIT (LENGTH_MEASURE( 1.000000000000000082E-05 ), #17598, 'distance_accuracy_value', 'NONE');
#7537=DIRECTION ( 'NONE',  ( 6.123230199561429643E-17, 4.868008300101910084E-15, 1.000000000000000000 ) ) ;
#7593=CARTESIAN_POINT ( 'NONE',  ( 35.09747506357100377, 11.43410645592859964, 29.25000000000000000 ) ) ;
#7596=ADVANCED_FACE ( 'NONE', ( #515 ), #8863, .F. ) ;
#7599=CARTESIAN_POINT ( 'NONE',  ( 35.59419854219520118, 9.774809681453550780, 26.68999999999999773 ) ) ;
#7601=ORIENTED_EDGE ( 'NONE', *, *, #22108, .T. ) ;
#7629=DIRECTION ( 'NONE',  ( 0.9730401042858022320, -0.2306359803922080343, 1.063156381331940328E-15 ) ) ;
#7633=VERTEX_POINT ( 'NONE', #22126 ) ;
#7708=AXIS2_PLACEMENT_3D ( 'NONE', #7418, #18462, #1931 ) ;
#7896=DIRECTION ( 'NONE',  ( -0.2306359803922102825, -0.9730401042858017879, 4.857225732735058287E-15 ) ) ;
#7937=EDGE_LOOP ( 'NONE', ( #19553, #2825, #13481, #17374, #8577, #22290 ) ) ;
#7956=ORIENTED_EDGE ( 'NONE', *, *, #10889, .F. ) ;
#7990=CIRCLE ( 'NONE', #3047, 2.009240000000000137 ) ;
#8016=CARTESIAN_POINT ( 'NONE',  ( 33.90884364377009774, 10.17428291754630010, 27.68999999999999773 ) ) ;
#8025=ORIENTED_EDGE ( 'NONE', *, *, #22281, .T. ) ;
#8042=CARTESIAN_POINT ( 'NONE',  ( 35.59419854219520118, 9.774809681453540122, 26.30000000000000071 ) ) ;
#8066=( BOUNDED_CURVE ( )  B_SPLINE_CURVE ( 2, ( #4237, #18755, #4476 ),
 .UNSPECIFIED., .F., .F. ) 
 B_SPLINE_CURVE_WITH_KNOTS ( ( 3, 3 ),
 ( 0.000000000000000000, 0.1752654207116860208 ),
 .UNSPECIFIED. ) 
 CURVE ( )  GEOMETRIC_REPRESENTATION_ITEM ( )  RATIONAL_B_SPLINE_CURVE ( ( 1.000000000000000000, 1.154700538379239916, 1.000000000000000000 ) ) 
 REPRESENTATION_ITEM ( '' )  );
#8074=CIRCLE ( 'NONE', #21344, 0.2000000000000016209 ) ;
#8090=VERTEX_POINT ( 'NONE', #13519 ) ;
#8105=CARTESIAN_POINT ( 'NONE',  ( 35.13079550495195491, 7.819738582318261244, 10.50000000000021139 ) ) ;
#8113=ADVANCED_FACE ( 'NONE', ( #4494, #10095 ), #18989, .T. ) ;
#8114=DIRECTION ( 'NONE',  ( -6.123230199561429643E-17, -4.868008300101910084E-15, -1.000000000000000000 ) ) ;
#8161=AXIS2_PLACEMENT_3D ( 'NONE', #15529, #19456, #10455 ) ;
#8163=ORIENTED_EDGE ( 'NONE', *, *, #1354, .F. ) ;
#8169=ORIENTED_EDGE ( 'NONE', *, *, #19869, .F. ) ;
#8195=CARTESIAN_POINT ( 'NONE',  ( 38.22140682376686982, 9.152092534394576262, 26.30000000000000426 ) ) ;
#8200=VERTEX_POINT ( 'NONE', #10457 ) ;
#8224=AXIS2_PLACEMENT_3D ( 'NONE', #4120, #18757, #17056 ) ;
#8246=CONICAL_SURFACE ( 'NONE', #2564, 0.8660254037844395958, 1.047197551196598297 ) ;
#8305=FACE_OUTER_BOUND ( 'NONE', #12603, .T. ) ;
#8494=VECTOR ( 'NONE', #6132, 1000.000000000000000 ) ;
#8566=( BOUNDED_CURVE ( )  B_SPLINE_CURVE ( 2, ( #8616, #14197, #15854 ),
 .UNSPECIFIED., .F., .F. ) 
 B_SPLINE_CURVE_WITH_KNOTS ( ( 3, 3 ),
 ( 0.08763271035584378754, 0.1752654207116860208 ),
 .UNSPECIFIED. ) 
 CURVE ( )  GEOMETRIC_REPRESENTATION_ITEM ( )  RATIONAL_B_SPLINE_CURVE ( ( 1.077350269189625065, 1.077350269189624399, 1.000000000000000000 ) ) 
 REPRESENTATION_ITEM ( '' )  );
#8577=ORIENTED_EDGE ( 'NONE', *, *, #14434, .T. ) ;
#8601=EDGE_CURVE ( 'NONE', #16298, #6737, #766, .T. ) ;
#8616=CARTESIAN_POINT ( 'NONE',  ( 35.24824457160688240, 8.315249525024842825, 27.55602540378454535 ) ) ;
#8629=CARTESIAN_POINT ( 'NONE',  ( 35.01760859121467462, 7.342209420738964987, 10.99076000000021125 ) ) ;
#8685=VERTEX_POINT ( 'NONE', #6369 ) ;
#8715=DIRECTION ( 'NONE',  ( -0.9730401042858020100, 0.2306359803922092278, -1.869849304631841307E-15 ) ) ;
#8810=CARTESIAN_POINT ( 'NONE',  ( 33.27836309399499015, 10.32372331478701533, 29.25000000000000000 ) ) ;
#8863=TOROIDAL_SURFACE ( 'NONE', #13791, 2.700000000000000178, 0.2000000000000000111 ) ;
#8928=ORIENTED_EDGE ( 'NONE', *, *, #15022, .F. ) ;
#8945=DIRECTION ( 'NONE',  ( 0.9579954394086682701, 0.2867834340965191298, -1.451283422213149430E-15 ) ) ;
#8952=LINE ( 'NONE', #3603, #444 ) ;
#8974=VECTOR ( 'NONE', #15416, 1000.000000000000000 ) ;
#9058=CARTESIAN_POINT ( 'NONE',  ( 33.90884364377009774, 10.17428291754630010, 27.68999999999999773 ) ) ;
#9062=CARTESIAN_POINT ( 'NONE',  ( 35.59419854219520118, 9.774809681453540122, 26.50000000000000000 ) ) ;
#9075=CARTESIAN_POINT ( 'NONE',  ( 35.59419854219520118, 9.774809681453559662, 29.25000000000000000 ) ) ;
#9145=DIRECTION ( 'NONE',  ( -6.123230199561459225E-17, -4.868008300101910084E-15, -1.000000000000000000 ) ) ;
#9179=DIRECTION ( 'NONE',  ( -0.2306359803922102825, -0.9730401042858017879, 4.163336342344335449E-15 ) ) ;
#9190=ORIENTED_EDGE ( 'NONE', *, *, #10887, .F. ) ;
#9251=CIRCLE ( 'NONE', #7001, 4.750000000000000000 ) ;
#9288=EDGE_CURVE ( 'NONE', #16446, #21387, #363, .T. ) ;
#9386=PRODUCT_DEFINITION ( 'UNKNOWN', '', #20866, #6623 ) ;
#9396=AXIS2_PLACEMENT_3D ( 'NONE', #20243, #14768, #16651 ) ;
#9453=ORIENTED_EDGE ( 'NONE', *, *, #10159, .F. ) ;
#9494=EDGE_CURVE ( 'NONE', #13130, #10377, #3474, .T. ) ;
#9547=EDGE_LOOP ( 'NONE', ( #112, #13363, #15709, #20166 ) ) ;
#9563=CARTESIAN_POINT ( 'NONE',  ( 35.59419854219520118, 9.774809681453540122, 26.30000000000000071 ) ) ;
#9646=EDGE_LOOP ( 'NONE', ( #14718, #13079, #3784, #12485, #3442 ) ) ;
#9783=LINE ( 'NONE', #17005, #19447 ) ;
#9793=LINE ( 'NONE', #20813, #12066 ) ;
#9798=DIRECTION ( 'NONE',  ( 3.959184095919419975E-16, -4.969292347292200534E-15, -1.000000000000000000 ) ) ;
#9828=EDGE_CURVE ( 'NONE', #17589, #16214, #7242, .T. ) ;
#9855=DIRECTION ( 'NONE',  ( 1.000000000000000000, -5.964507377817269296E-17, 0.000000000000000000 ) ) ;
#9992=LINE ( 'NONE', #2157, #8974 ) ;
#10057=EDGE_LOOP ( 'NONE', ( #2496, #2473, #15546, #23286, #15696, #21228 ) ) ;
#10058=ORIENTED_EDGE ( 'NONE', *, *, #7511, .F. ) ;
#10095=FACE_OUTER_BOUND ( 'NONE', #5450, .T. ) ;
#10109=ORIENTED_EDGE ( 'NONE', *, *, #14311, .F. ) ;
#10125=EDGE_CURVE ( 'NONE', #3393, #8685, #8066, .T. ) ;
#10159=EDGE_CURVE ( 'NONE', #17438, #13418, #12548, .T. ) ;
#10209=CIRCLE ( 'NONE', #11354, 2.500000000000000888 ) ;
#10344=ORIENTED_EDGE ( 'NONE', *, *, #15022, .T. ) ;
#10372=DIRECTION ( 'NONE',  ( -0.2306359803922084506, -0.9730401042858020100, 5.112869192352694760E-15 ) ) ;
#10377=VERTEX_POINT ( 'NONE', #8629 ) ;
#10455=DIRECTION ( 'NONE',  ( -0.9730401042858020100, 0.2306359803922089780, 0.000000000000000000 ) ) ;
#10457=CARTESIAN_POINT ( 'NONE',  ( 33.90884364377009774, 10.17428291754630010, 29.25000000000000000 ) ) ;
#10488=CARTESIAN_POINT ( 'NONE',  ( 34.49867763533220710, 5.152869186095990095, 26.88000000000002387 ) ) ;
#10493=EDGE_LOOP ( 'NONE', ( #1315, #1706, #20406, #19105, #1477 ) ) ;
#10494=EDGE_LOOP ( 'NONE', ( #8928, #5075, #7956, #7348, #16534 ) ) ;
#10518=EDGE_CURVE ( 'NONE', #8685, #1899, #20334, .T. ) ;
#10520=FACE_OUTER_BOUND ( 'NONE', #23043, .T. ) ;
#10548=TOROIDAL_SURFACE ( 'NONE', #9396, 2.700000000000000178, 0.2000000000000000111 ) ;
#10586=AXIS2_PLACEMENT_3D ( 'NONE', #12744, #8945, #12633 ) ;
#10689=EDGE_LOOP ( 'NONE', ( #19754, #3190, #13460, #17331, #16873 ) ) ;
#10700=ORIENTED_EDGE ( 'NONE', *, *, #21508, .T. ) ;
#10716=FACE_OUTER_BOUND ( 'NONE', #13164, .T. ) ;
#10793=VERTEX_POINT ( 'NONE', #1452 ) ;
#10816=ADVANCED_FACE ( 'NONE', ( #3359 ), #15924, .T. ) ;
#10836=CARTESIAN_POINT ( 'NONE',  ( 35.01760859121468172, 7.342209420738994297, 17.70000000000000995 ) ) ;
#10869=DIRECTION ( 'NONE',  ( 6.052506032659479608E-17, 4.865024487662030352E-15, 1.000000000000000000 ) ) ;
#10887=EDGE_CURVE ( 'NONE', #15962, #8685, #16414, .T. ) ;
#10889=EDGE_CURVE ( 'NONE', #18259, #23367, #20738, .T. ) ;
#10950=AXIS2_PLACEMENT_3D ( 'NONE', #12009, #19342, #19230 ) ;
#10956=FACE_OUTER_BOUND ( 'NONE', #10494, .T. ) ;
#10962=EDGE_CURVE ( 'NONE', #21387, #16446, #7474, .T. ) ;
#10994=( BOUNDED_CURVE ( )  B_SPLINE_CURVE ( 2, ( #9058, #11, #14175 ),
 .UNSPECIFIED., .F., .F. ) 
 B_SPLINE_CURVE_WITH_KNOTS ( ( 3, 3 ),
 ( 0.000000000000000000, 0.1752654207116860208 ),
 .UNSPECIFIED. ) 
 CURVE ( )  GEOMETRIC_REPRESENTATION_ITEM ( )  RATIONAL_B_SPLINE_CURVE ( ( 1.000000000000000000, 1.154700538379239916, 1.000000000000000000 ) ) 
 REPRESENTATION_ITEM ( '' )  );
#11090=CARTESIAN_POINT ( 'NONE',  ( 35.07420204808331476, 7.580974001528614004, 10.74538000000021043 ) ) ;
#11104=FACE_OUTER_BOUND ( 'NONE', #11107, .T. ) ;
#11107=EDGE_LOOP ( 'NONE', ( #9453, #10344, #20545, #2905, #469 ) ) ;
#11166=CARTESIAN_POINT ( 'NONE',  ( 37.15537257096429613, 9.790160638979559238, 29.25000000000000000 ) ) ;
#11189=EDGE_CURVE ( 'NONE', #6737, #15927, #22625, .T. ) ;
#11193=CONICAL_SURFACE ( 'NONE', #15330, 2.254620000000000513, 0.7853981633974461696 ) ;
#11222=EDGE_CURVE ( 'NONE', #16298, #16051, #15077, .T. ) ;
#11259=CARTESIAN_POINT ( 'NONE',  ( 36.33124047800322387, 11.14167175084476824, 27.55602540378454535 ) ) ;
#11354=AXIS2_PLACEMENT_3D ( 'NONE', #5602, #12848, #20083 ) ;
#11363=CLOSED_SHELL ( 'NONE', ( #14956, #11845, #5496, #17979, #19221, #7596, #22397, #16518, #20698, #14418, #14928, #10816, #8113, #19106, #6769, #15093, #4047, #12854, #23143, #23296, #12686 ) ) ;
#11430=ORIENTED_EDGE ( 'NONE', *, *, #19869, .T. ) ;
#11455=CARTESIAN_POINT ( 'NONE',  ( 35.59419854219520118, 9.774809681453540122, 26.50000000000000000 ) ) ;
#11487=CARTESIAN_POINT ( 'NONE',  ( 36.78282996199610722, 11.03463321983590006, 29.25000000000000000 ) ) ;
#11597=DIRECTION ( 'NONE',  ( -0.2867834340965179085, 0.9579954394086686031, -4.640009386119478376E-15 ) ) ;
#11610=DIRECTION ( 'NONE',  ( 0.2306359803922080620, 0.9730401042858023430, -4.744007713284279563E-15 ) ) ;
#11628=ORIENTED_EDGE ( 'NONE', *, *, #17355, .T. ) ;
#11720=FACE_OUTER_BOUND ( 'NONE', #9646, .T. ) ;
#11732=EDGE_CURVE ( 'NONE', #8200, #8090, #20194, .T. ) ;
#11821=FACE_OUTER_BOUND ( 'NONE', #7937, .T. ) ;
#11845=ADVANCED_FACE ( 'NONE', ( #8305 ), #15540, .T. ) ;
#11928=CARTESIAN_POINT ( 'NONE',  ( 33.27836309399499015, 10.32372331478700644, 26.87999999999999901 ) ) ;
#12009=CARTESIAN_POINT ( 'NONE',  ( 35.59419854219520118, 9.774809681453550780, 27.87500000000000000 ) ) ;
#12020=PLANE ( 'NONE',  #16774 ) ;
#12066=VECTOR ( 'NONE', #11597, 1000.000000000000114 ) ;
#12068=ORIENTED_EDGE ( 'NONE', *, *, #1712, .T. ) ;
#12082=AXIS2_PLACEMENT_3D ( 'NONE', #9563, #15008, #13002 ) ;
#12208=ORIENTED_EDGE ( 'NONE', *, *, #17900, .F. ) ;
#12234=ORIENTED_EDGE ( 'NONE', *, *, #9494, .F. ) ;
#12242=FACE_OUTER_BOUND ( 'NONE', #4367, .T. ) ;
#12318=ORIENTED_EDGE ( 'NONE', *, *, #9288, .T. ) ;
#12376=DIRECTION ( 'NONE',  ( 0.2306359803922101437, 0.9730401042858017879, -4.006172263299087069E-15 ) ) ;
#12383=VERTEX_POINT ( 'NONE', #3268 ) ;
#12401=CARTESIAN_POINT ( 'NONE',  ( 36.78282996199610722, 11.03463321983590006, 29.25000000000000000 ) ) ;
#12432=AXIS2_PLACEMENT_3D ( 'NONE', #22217, #1189, #10372 ) ;
#12437=AXIS2_PLACEMENT_3D ( 'NONE', #9075, #5057, #17761 ) ;
#12480=EDGE_CURVE ( 'NONE', #23367, #17438, #1429, .T. ) ;
#12485=ORIENTED_EDGE ( 'NONE', *, *, #6999, .F. ) ;
#12524=ORIENTED_EDGE ( 'NONE', *, *, #7182, .T. ) ;
#12548=CIRCLE ( 'NONE', #16690, 2.500000000000000888 ) ;
#12603=EDGE_LOOP ( 'NONE', ( #2166, #6119, #2513, #13328, #10058 ) ) ;
#12605=CARTESIAN_POINT ( 'NONE',  ( 35.88249351768550355, 10.99110981181069846, 10.50000000000020073 ) ) ;
#12633=DIRECTION ( 'NONE',  ( 0.000000000000000000, -5.060555282020610014E-15, -1.000000000000000000 ) ) ;
#12637=FACE_OUTER_BOUND ( 'NONE', #7262, .T. ) ;
#12641=DIRECTION ( 'NONE',  ( -5.964507377817318600E-17, -4.861311874385510251E-15, -1.000000000000000000 ) ) ;
#12643=CARTESIAN_POINT ( 'NONE',  ( 36.68971944905818816, 14.39675017681109992, 26.49999999999997513 ) ) ;
#12655=FACE_BOUND ( 'NONE', #5118, .T. ) ;
#12686=ADVANCED_FACE ( 'NONE', ( #11821 ), #19281, .F. ) ;
#12739=AXIS2_PLACEMENT_3D ( 'NONE', #2569, #13380, #415 ) ;
#12744=CARTESIAN_POINT ( 'NONE',  ( 37.27955344062029752, 9.375336445360789028, 29.25000000000000000 ) ) ;
#12835=ORIENTED_EDGE ( 'NONE', *, *, #10518, .F. ) ;
#12848=DIRECTION ( 'NONE',  ( -6.123230199561459225E-17, -4.868008300101910084E-15, -1.000000000000000000 ) ) ;
#12854=ADVANCED_FACE ( 'NONE', ( #14049 ), #14521, .F. ) ;
#12883=CARTESIAN_POINT ( 'NONE',  ( 36.78282996199610722, 11.03463321983590006, 27.68999999999999773 ) ) ;
#12942=DIRECTION ( 'NONE',  ( 0.6862566701892842680, 0.7273594590164591533, -3.576853004787541598E-15 ) ) ;
#13002=DIRECTION ( 'NONE',  ( -0.2306359803922102825, -0.9730401042858017879, 4.163336342344335449E-15 ) ) ;
#13018=VECTOR ( 'NONE', #13226, 1000.000000000000000 ) ;
#13043=EDGE_CURVE ( 'NONE', #10377, #18172, #10209, .T. ) ;
#13048=LINE ( 'NONE', #20162, #16544 ) ;
#13054=CARTESIAN_POINT ( 'NONE',  ( 36.17078849317572065, 12.20740994216797404, 10.99076000000018816 ) ) ;
#13079=ORIENTED_EDGE ( 'NONE', *, *, #15900, .T. ) ;
#13130=VERTEX_POINT ( 'NONE', #8105 ) ;
#13164=EDGE_LOOP ( 'NONE', ( #12208, #10700, #8025, #18781, #21206, #16807 ) ) ;
#13226=DIRECTION ( 'NONE',  ( 5.964507377817269296E-17, 4.861311874385510251E-15, 1.000000000000000000 ) ) ;
#13243=ORIENTED_EDGE ( 'NONE', *, *, #14874, .F. ) ;
#13290=EDGE_CURVE ( 'NONE', #2844, #15962, #18031, .T. ) ;
#13328=ORIENTED_EDGE ( 'NONE', *, *, #1127, .F. ) ;
#13363=ORIENTED_EDGE ( 'NONE', *, *, #19389, .T. ) ;
#13369=AXIS2_PLACEMENT_3D ( 'NONE', #19605, #23151, #21390 ) ;
#13380=DIRECTION ( 'NONE',  ( 0.000000000000000000, 0.000000000000000000, 1.000000000000000000 ) ) ;
#13407=EDGE_LOOP ( 'NONE', ( #20989, #7601, #8163, #1264 ) ) ;
#13418=VERTEX_POINT ( 'NONE', #2213 ) ;
#13460=ORIENTED_EDGE ( 'NONE', *, *, #5192, .T. ) ;
#13481=ORIENTED_EDGE ( 'NONE', *, *, #22183, .T. ) ;
#13519=CARTESIAN_POINT ( 'NONE',  ( 35.09747506357100377, 11.43410645592859964, 29.25000000000000000 ) ) ;
#13558=CIRCLE ( 'NONE', #15065, 2.009240000000000137 ) ;
#13583=CARTESIAN_POINT ( 'NONE',  ( 35.59419854219520118, 9.774809681453550780, 26.88000000000000256 ) ) ;
#13630=VERTEX_POINT ( 'NONE', #5067 ) ;
#13657=FACE_OUTER_BOUND ( 'NONE', #13407, .T. ) ;
#13686=ORIENTED_EDGE ( 'NONE', *, *, #9288, .F. ) ;
#13698=DIRECTION ( 'NONE',  ( 6.123230199561449365E-17, 4.868008300101910084E-15, 1.000000000000000000 ) ) ;
#13741=CARTESIAN_POINT ( 'NONE',  ( 34.40556712239430226, 8.514986143071229918, 27.68999999999999773 ) ) ;
#13791=AXIS2_PLACEMENT_3D ( 'NONE', #15560, #9798, #17020 ) ;
#13817=VECTOR ( 'NONE', #2956, 1000.000000000000000 ) ;
#13971=EDGE_LOOP ( 'NONE', ( #16894, #16609, #2465, #7030 ) ) ;
#14049=FACE_OUTER_BOUND ( 'NONE', #6149, .T. ) ;
#14060=CYLINDRICAL_SURFACE ( 'NONE', #20609, 4.750000000000000000 ) ;
#14134=AXIS2_PLACEMENT_3D ( 'NONE', #11487, #11610, #20608 ) ;
#14175=CARTESIAN_POINT ( 'NONE',  ( 34.40556712239430226, 8.514986143071229918, 27.68999999999999773 ) ) ;
#14197=CARTESIAN_POINT ( 'NONE',  ( 35.63933253682658631, 8.222551437987361211, 27.55602540378454535 ) ) ;
#14250=ORIENTED_EDGE ( 'NONE', *, *, #8601, .F. ) ;
#14278=APPLICATION_CONTEXT ( 'configuration controlled 3d designs of mechanical parts and assemblies' ) ;
#14311=EDGE_CURVE ( 'NONE', #16214, #16298, #18091, .T. ) ;
#14370=PLANE ( 'NONE',  #3691 ) ;
#14418=ADVANCED_FACE ( 'NONE', ( #12637 ), #16562, .T. ) ;
#14434=EDGE_CURVE ( 'NONE', #14944, #10793, #10994, .T. ) ;
#14441=CARTESIAN_POINT ( 'NONE',  ( 35.94015251278350576, 11.23436983788223209, 27.55602540378454179 ) ) ;
#14462=DIRECTION ( 'NONE',  ( -0.1997366180463828189, -0.8426774492125620464, 0.5000000000000035527 ) ) ;
#14489=CARTESIAN_POINT ( 'NONE',  ( 35.59419854219520118, 9.774809681453550780, 27.18999999999999773 ) ) ;
#14520=ORIENTED_EDGE ( 'NONE', *, *, #17707, .T. ) ;
#14521=PLANE ( 'NONE',  #10586 ) ;
#14528=CARTESIAN_POINT ( 'NONE',  ( 34.40556712239430226, 8.514986143071238800, 29.25000000000000000 ) ) ;
#14536=CYLINDRICAL_SURFACE ( 'NONE', #3535, 2.500000000000000888 ) ;
#14703=DIRECTION ( 'NONE',  ( 5.964507377817269296E-17, 4.861311874385510251E-15, 1.000000000000000000 ) ) ;
#14717=PLANE ( 'NONE',  #19036 ) ;
#14718=ORIENTED_EDGE ( 'NONE', *, *, #20158, .F. ) ;
#14743=VECTOR ( 'NONE', #18387, 1000.000000000000114 ) ;
#14768=DIRECTION ( 'NONE',  ( 3.959184095919419975E-16, -4.969292347292200534E-15, -1.000000000000000000 ) ) ;
#14813=LINE ( 'NONE', #16948, #18687 ) ;
#14874=EDGE_CURVE ( 'NONE', #13130, #7633, #13558, .T. ) ;
#14928=ADVANCED_FACE ( 'NONE', ( #21490 ), #14370, .T. ) ;
#14931=ORIENTED_EDGE ( 'NONE', *, *, #11189, .F. ) ;
#14944=VERTEX_POINT ( 'NONE', #7144 ) ;
#14956=ADVANCED_FACE ( 'NONE', ( #10716 ), #8246, .F. ) ;
#14972=CARTESIAN_POINT ( 'NONE',  ( 38.22140682376686982, 9.152092534394578038, 26.50000000000000355 ) ) ;
#15008=DIRECTION ( 'NONE',  ( 6.123230199561459225E-17, 4.868008300101910084E-15, 1.000000000000000000 ) ) ;
#15012=CARTESIAN_POINT ( 'NONE',  ( 35.09747506357100377, 11.43410645592859964, 27.68999999999999773 ) ) ;
#15019=DIRECTION ( 'NONE',  ( -0.9730401042858020100, 0.2306359803922092278, -1.869849304631841307E-15 ) ) ;
#15022=EDGE_CURVE ( 'NONE', #17438, #10377, #18171, .T. ) ;
#15065=AXIS2_PLACEMENT_3D ( 'NONE', #1065, #6426, #20910 ) ;
#15077=CIRCLE ( 'NONE', #12432, 4.750000000000000000 ) ;
#15093=ADVANCED_FACE ( 'NONE', ( #2239 ), #14717, .F. ) ;
#15151=DIRECTION ( 'NONE',  ( -0.2306359803922102825, -0.9730401042858017879, 4.163336342344335449E-15 ) ) ;
#15203=( BOUNDED_CURVE ( )  B_SPLINE_CURVE ( 2, ( #22858, #6723, #21190 ),
 .UNSPECIFIED., .F., .F. ) 
 B_SPLINE_CURVE_WITH_KNOTS ( ( 3, 3 ),
 ( 0.08763271035584448143, 0.1752654207116860208 ),
 .UNSPECIFIED. ) 
 CURVE ( )  GEOMETRIC_REPRESENTATION_ITEM ( )  RATIONAL_B_SPLINE_CURVE ( ( 1.077350269189624843, 1.077350269189623511, 1.000000000000000000 ) ) 
 REPRESENTATION_ITEM ( '' )  );
#15264=CIRCLE ( 'NONE', #16002, 2.379999999999999893 ) ;
#15294=ORIENTED_EDGE ( 'NONE', *, *, #11189, .T. ) ;
#15330=AXIS2_PLACEMENT_3D ( 'NONE', #19816, #3074, #5102 ) ;
#15407=PLANE ( 'NONE',  #8161 ) ;
#15416=DIRECTION ( 'NONE',  ( 0.1630842657209383706, 0.6880432561069579345, 0.7071067811865456854 ) ) ;
#15425=DIRECTION ( 'NONE',  ( 0.2306359803922089224, 0.9730401042858022320, -4.744007713284279563E-15 ) ) ;
#15432=AXIS2_PLACEMENT_3D ( 'NONE', #9062, #12641, #14 ) ;
#15460=ORIENTED_EDGE ( 'NONE', *, *, #3000, .F. ) ;
#15527=PRODUCT ( 'Pin 2', 'Pin 2', '', ( #6516 ) ) ;
#15529=CARTESIAN_POINT ( 'NONE',  ( 34.40556712239430226, 8.514986143071238800, 29.25000000000000000 ) ) ;
#15540=CYLINDRICAL_SURFACE ( 'NONE', #10950, 4.750000000000000000 ) ;
#15546=ORIENTED_EDGE ( 'NONE', *, *, #16881, .T. ) ;
#15560=CARTESIAN_POINT ( 'NONE',  ( 35.59419854219520118, 9.774809681453540122, 26.30000000000000071 ) ) ;
#15565=DIRECTION ( 'NONE',  ( -0.2306359803922090335, -0.9730401042858022320, 4.744007713284281141E-15 ) ) ;
#15676=DIRECTION ( 'NONE',  ( -0.9730401042858026761, 0.2306359803922063967, 0.000000000000000000 ) ) ;
#15678=ORIENTED_EDGE ( 'NONE', *, *, #3000, .T. ) ;
#15696=ORIENTED_EDGE ( 'NONE', *, *, #1354, .T. ) ;
#15709=ORIENTED_EDGE ( 'NONE', *, *, #16881, .F. ) ;
#15719=DIRECTION ( 'NONE',  ( 0.2306359803922101437, 0.9730401042858017879, -4.006172263299087069E-15 ) ) ;
#15801=VECTOR ( 'NONE', #23417, 1000.000000000000000 ) ;
#15854=CARTESIAN_POINT ( 'NONE',  ( 36.09092202081949807, 8.115512906978459284, 27.68999999999999773 ) ) ;
#15900=EDGE_CURVE ( 'NONE', #1899, #2844, #8952, .T. ) ;
#15903=CARTESIAN_POINT ( 'NONE',  ( 33.90884364377009774, 10.17428291754630010, 29.25000000000000000 ) ) ;
#15922=CYLINDRICAL_SURFACE ( 'NONE', #13369, 2.500000000000000888 ) ;
#15924=TOROIDAL_SURFACE ( 'NONE', #5677, 2.380000000000000338, 2.370000000000000107 ) ;
#15927=VERTEX_POINT ( 'NONE', #12643 ) ;
#15962=VERTEX_POINT ( 'NONE', #2051 ) ;
#15994=VERTEX_POINT ( 'NONE', #14528 ) ;
#16002=AXIS2_PLACEMENT_3D ( 'NONE', #22531, #18871, #22288 ) ;
#16038=DIRECTION ( 'NONE',  ( -5.964507377817269296E-17, -4.861311874385510251E-15, -1.000000000000000000 ) ) ;
#16051=VERTEX_POINT ( 'NONE', #17858 ) ;
#16116=PRODUCT_DEFINITION_SHAPE ( 'NONE', 'NONE',  #9386 ) ;
#16214=VERTEX_POINT ( 'NONE', #22335 ) ;
#16298=VERTEX_POINT ( 'NONE', #10488 ) ;
#16306=ORIENTED_EDGE ( 'NONE', *, *, #9494, .T. ) ;
#16343=FACE_OUTER_BOUND ( 'NONE', #9547, .T. ) ;
#16410=DIRECTION ( 'NONE',  ( -0.1630842657209382041, -0.6880432561069511621, 0.7071067811865524577 ) ) ;
#16414=LINE ( 'NONE', #5720, #17348 ) ;
#16446=VERTEX_POINT ( 'NONE', #7261 ) ;
#16454=ORIENTED_EDGE ( 'NONE', *, *, #5192, .F. ) ;
#16470=ORIENTED_EDGE ( 'NONE', *, *, #1712, .F. ) ;
#16518=ADVANCED_FACE ( 'NONE', ( #10956 ), #15922, .T. ) ;
#16534=ORIENTED_EDGE ( 'NONE', *, *, #13043, .F. ) ;
#16544=VECTOR ( 'NONE', #14462, 999.9999999999998863 ) ;
#16550=CARTESIAN_POINT ( 'NONE',  ( 37.03119170130820237, 10.20498483259830280, 27.44000000000020378 ) ) ;
#16562=CONICAL_SURFACE ( 'NONE', #6340, 2.254620000000000513, 0.7853981633974461696 ) ;
#16579=CARTESIAN_POINT ( 'NONE',  ( 36.09092202081949807, 8.115512906978459284, 27.68999999999999773 ) ) ;
#16609=ORIENTED_EDGE ( 'NONE', *, *, #6999, .T. ) ;
#16638=ORIENTED_EDGE ( 'NONE', *, *, #14874, .T. ) ;
#16644=VERTEX_POINT ( 'NONE', #7599 ) ;
#16651=DIRECTION ( 'NONE',  ( -0.9730401042858021210, 0.2306359803922091167, -1.531342102931250897E-15 ) ) ;
#16690=AXIS2_PLACEMENT_3D ( 'NONE', #8042, #4591, #15151 ) ;
#16774=AXIS2_PLACEMENT_3D ( 'NONE', #15903, #1173, #17456 ) ;
#16797=CARTESIAN_POINT ( 'NONE',  ( 34.50315935367051878, 10.80419468673749606, 27.44000000000020378 ) ) ;
#16807=ORIENTED_EDGE ( 'NONE', *, *, #20158, .T. ) ;
#16825=VECTOR ( 'NONE', #20745, 1000.000000000000227 ) ;
#16873=ORIENTED_EDGE ( 'NONE', *, *, #7182, .F. ) ;
#16881=EDGE_CURVE ( 'NONE', #15962, #2620, #2849, .T. ) ;
#16894=ORIENTED_EDGE ( 'NONE', *, *, #2518, .F. ) ;
#16914=DIRECTION ( 'NONE',  ( -6.123230199561459225E-17, -4.868008300101910084E-15, -1.000000000000000000 ) ) ;
#16939=MANIFOLD_SOLID_BREP ( 'Imported1', #11363 ) ;
#16948=CARTESIAN_POINT ( 'NONE',  ( 36.17078849317572775, 12.20740994216800601, 17.69999999999998863 ) ) ;
#16962=CIRCLE ( 'NONE', #12437, 2.379999999999999893 ) ;
#17005=CARTESIAN_POINT ( 'NONE',  ( 36.36149123738979938, 11.13450152885909894, 29.25000000000000000 ) ) ;
#17020=DIRECTION ( 'NONE',  ( -0.9730401042858021210, 0.2306359803922091167, -1.531342102931250897E-15 ) ) ;
#17041=DIRECTION ( 'NONE',  ( 5.964507377817269296E-17, 4.861311874385510251E-15, 1.000000000000000000 ) ) ;
#17049=CARTESIAN_POINT ( 'NONE',  ( 34.49867763533220710, 5.152869186095990983, 27.87500000000002487 ) ) ;
#17056=DIRECTION ( 'NONE',  ( -0.2306359803922102825, -0.9730401042858017879, 4.163336342344335449E-15 ) ) ;
#17170=CARTESIAN_POINT ( 'NONE',  ( 33.90884364377009774, 10.17428291754630010, 28.46999999999999886 ) ) ;
#17171=APPLICATION_CONTEXT ( 'configuration controlled 3d designs of mechanical parts and assemblies' ) ;
#17230=LINE ( 'NONE', #4626, #13817 ) ;
#17331=ORIENTED_EDGE ( 'NONE', *, *, #10962, .T. ) ;
#17348=VECTOR ( 'NONE', #1692, 1000.000000000000000 ) ;
#17355=EDGE_CURVE ( 'NONE', #18172, #10377, #23256, .T. ) ;
#17366=CARTESIAN_POINT ( 'NONE',  ( 35.59419854219520118, 9.774809681453469068, 10.99076000000020059 ) ) ;
#17374=ORIENTED_EDGE ( 'NONE', *, *, #2518, .T. ) ;
#17402=CARTESIAN_POINT ( 'NONE',  ( 35.59419854219520118, 9.774809681453550780, 27.87500000000000000 ) ) ;
#17438=VERTEX_POINT ( 'NONE', #7147 ) ;
#17456=DIRECTION ( 'NONE',  ( -0.2867834340965179085, 0.9579954394086686031, 0.000000000000000000 ) ) ;
#17589=VERTEX_POINT ( 'NONE', #8810 ) ;
#17598=( LENGTH_UNIT ( ) NAMED_UNIT ( * ) SI_UNIT ( .MILLI., .METRE. ) );
#17694=ORIENTED_EDGE ( 'NONE', *, *, #1127, .T. ) ;
#17707=EDGE_CURVE ( 'NONE', #13630, #16214, #9251, .T. ) ;
#17761=DIRECTION ( 'NONE',  ( -0.2306359803922101437, -0.9730401042858018990, 4.373252460445732608E-15 ) ) ;
#17838=EDGE_LOOP ( 'NONE', ( #11430, #2637, #17924, #14520, #17896 ) ) ;
#17858=CARTESIAN_POINT ( 'NONE',  ( 40.21613903755275743, 8.679288774590558475, 26.88000000000000611 ) ) ;
#17896=ORIENTED_EDGE ( 'NONE', *, *, #9828, .F. ) ;
#17900=EDGE_CURVE ( 'NONE', #16644, #23121, #17230, .T. ) ;
#17924=ORIENTED_EDGE ( 'NONE', *, *, #7511, .T. ) ;
#17946=EDGE_CURVE ( 'NONE', #15927, #6737, #3953, .T. ) ;
#17979=ADVANCED_FACE ( 'NONE', ( #12242 ), #11193, .T. ) ;
#18031=LINE ( 'NONE', #11166, #14743 ) ;
#18051=SHAPE_REPRESENTATION_RELATIONSHIP ( 'NONE' , 'NONE' ,  #7508, #1704 ) ;
#18088=CIRCLE ( 'NONE', #8224, 2.500000000000000888 ) ;
#18091=CIRCLE ( 'NONE', #2544, 4.750000000000000000 ) ;
#18144=CARTESIAN_POINT ( 'NONE',  ( 36.09092202081949807, 8.115512906978469942, 29.25000000000000000 ) ) ;
#18171=LINE ( 'NONE', #10836, #21890 ) ;
#18172=VERTEX_POINT ( 'NONE', #13054 ) ;
#18238=EDGE_CURVE ( 'NONE', #18259, #18172, #14813, .T. ) ;
#18244=DIRECTION ( 'NONE',  ( -0.9730401042858020100, 0.2306359803922089780, 0.000000000000000000 ) ) ;
#18256=DIRECTION ( 'NONE',  ( -4.590283530086319968E-31, -4.798094407101261014E-15, -1.000000000000000000 ) ) ;
#18259=VERTEX_POINT ( 'NONE', #779 ) ;
#18337=EDGE_CURVE ( 'NONE', #2620, #15994, #2696, .T. ) ;
#18387=DIRECTION ( 'NONE',  ( 0.2867834340965190743, -0.9579954394086682701, 4.640009386119481531E-15 ) ) ;
#18462=DIRECTION ( 'NONE',  ( -5.964507377817269296E-17, -4.861311874385510251E-15, -1.000000000000000000 ) ) ;
#18476=CARTESIAN_POINT ( 'NONE',  ( 37.27955344062029752, 9.375336445360778370, 27.68999999999999773 ) ) ;
#18483=AXIS2_PLACEMENT_3D ( 'NONE', #11455, #8114, #6076 ) ;
#18492=VECTOR ( 'NONE', #20241, 1000.000000000000000 ) ;
#18554=DIRECTION ( 'NONE',  ( 5.964507377817298878E-17, 4.861311874385510251E-15, 1.000000000000000000 ) ) ;
#18579=CARTESIAN_POINT ( 'NONE',  ( 37.91003399039540511, 9.225896048120105775, 29.25000000000000355 ) ) ;
#18687=VECTOR ( 'NONE', #19102, 1000.000000000000000 ) ;
#18707=FACE_OUTER_BOUND ( 'NONE', #3889, .T. ) ;
#18713=DIRECTION ( 'NONE',  ( -0.2306359803922084506, -0.9730401042858020100, 5.112869192352694760E-15 ) ) ;
#18718=VECTOR ( 'NONE', #14703, 1000.000000000000000 ) ;
#18755=CARTESIAN_POINT ( 'NONE',  ( 36.68523773071988359, 8.745424676169610834, 27.44000000000022865 ) ) ;
#18757=DIRECTION ( 'NONE',  ( 6.123230199561459225E-17, 4.868008300101910084E-15, 1.000000000000000000 ) ) ;
#18781=ORIENTED_EDGE ( 'NONE', *, *, #10125, .T. ) ;
#18829=( BOUNDED_CURVE ( )  B_SPLINE_CURVE ( 2, ( #15012, #16797, #8016 ),
 .UNSPECIFIED., .F., .F. ) 
 B_SPLINE_CURVE_WITH_KNOTS ( ( 3, 3 ),
 ( 0.000000000000000000, 0.1752654207116860208 ),
 .UNSPECIFIED. ) 
 CURVE ( )  GEOMETRIC_REPRESENTATION_ITEM ( )  RATIONAL_B_SPLINE_CURVE ( ( 1.000000000000000000, 1.154700538379249908, 1.000000000000000000 ) ) 
 REPRESENTATION_ITEM ( '' )  );
#18871=DIRECTION ( 'NONE',  ( -5.964507377817349415E-17, -4.861311874385510251E-15, -1.000000000000000000 ) ) ;
#18989=PLANE ( 'NONE',  #21346 ) ;
#19012=CARTESIAN_POINT ( 'NONE',  ( 34.49867763533220710, 5.152869186095979437, 26.50000000000002487 ) ) ;
#19036=AXIS2_PLACEMENT_3D ( 'NONE', #7593, #5930, #2125 ) ;
#19054=CARTESIAN_POINT ( 'NONE',  ( 35.59419854219520118, 9.774809681453550780, 27.18999999999999773 ) ) ;
#19102=DIRECTION ( 'NONE',  ( -6.123230199561459225E-17, -4.868008300101910084E-15, -1.000000000000000000 ) ) ;
#19105=ORIENTED_EDGE ( 'NONE', *, *, #14311, .T. ) ;
#19106=ADVANCED_FACE ( 'NONE', ( #10520 ), #14060, .T. ) ;
#19133=CARTESIAN_POINT ( 'NONE',  ( 36.38807987576970504, 8.430468791574050158, 29.25000000000000000 ) ) ;
#19207=EDGE_LOOP ( 'NONE', ( #1870, #15294 ) ) ;
#19221=ADVANCED_FACE ( 'NONE', ( #11104 ), #14536, .T. ) ;
#19230=DIRECTION ( 'NONE',  ( 0.2306359803922084506, 0.9730401042858022320, -5.112869192352694760E-15 ) ) ;
#19281=CONICAL_SURFACE ( 'NONE', #6000, 0.8660254037844395958, 1.047197551196598297 ) ;
#19342=DIRECTION ( 'NONE',  ( -6.123230199561449365E-17, -4.868008300101910084E-15, -1.000000000000000000 ) ) ;
#19389=EDGE_CURVE ( 'NONE', #3393, #2620, #20694, .T. ) ;
#19447=VECTOR ( 'NONE', #7629, 1000.000000000000227 ) ;
#19456=DIRECTION ( 'NONE',  ( -0.2306359803922090057, -0.9730401042858021210, 4.744007713284281930E-15 ) ) ;
#19553=ORIENTED_EDGE ( 'NONE', *, *, #21508, .F. ) ;
#19580=DIRECTION ( 'NONE',  ( 0.2306359803922084506, 0.9730401042858022320, -5.112869192352694760E-15 ) ) ;
#19601=DIRECTION ( 'NONE',  ( 3.764133351409869857E-47, -1.000000000000000000, 4.861311874385510251E-15 ) ) ;
#19605=CARTESIAN_POINT ( 'NONE',  ( 35.59419854219520118, 9.774809681453501042, 17.69999999999999929 ) ) ;
#19741=AXIS2_PLACEMENT_3D ( 'NONE', #22251, #2668, #15019 ) ;
#19754=ORIENTED_EDGE ( 'NONE', *, *, #12480, .T. ) ;
#19816=CARTESIAN_POINT ( 'NONE',  ( 35.59419854219520118, 9.774809681453469068, 10.74538000000019977 ) ) ;
#19823=CARTESIAN_POINT ( 'NONE',  ( 35.09747506357100377, 11.43410645592859964, 28.46999999999999886 ) ) ;
#19869=EDGE_CURVE ( 'NONE', #17589, #20801, #15264, .T. ) ;
#19886=CARTESIAN_POINT ( 'NONE',  ( 35.59419854219520118, 9.774809681453501042, 17.69999999999999929 ) ) ;
#19891=LINE ( 'NONE', #3614, #18492 ) ;
#20031=DIRECTION ( 'NONE',  ( 0.7273594590164591533, -0.6862566701892842680, 3.292724291071139008E-15 ) ) ;
#20083=DIRECTION ( 'NONE',  ( -0.2306359803922102825, -0.9730401042858017879, 4.857225732735058287E-15 ) ) ;
#20158=EDGE_CURVE ( 'NONE', #1899, #23121, #6115, .T. ) ;
#20162=CARTESIAN_POINT ( 'NONE',  ( 35.39446192414881409, 8.932132232240984848, 27.19000000000000128 ) ) ;
#20166=ORIENTED_EDGE ( 'NONE', *, *, #10887, .T. ) ;
#20194=LINE ( 'NONE', #5686, #5228 ) ;
#20241=DIRECTION ( 'NONE',  ( -6.123230199561449365E-17, -4.868008300101910084E-15, -1.000000000000000000 ) ) ;
#20243=CARTESIAN_POINT ( 'NONE',  ( 35.59419854219520118, 9.774809681453540122, 26.30000000000000071 ) ) ;
#20247=CARTESIAN_POINT ( 'NONE',  ( 35.59419854219520118, 9.774809681453550780, 26.88000000000000256 ) ) ;
#20289=ORIENTED_EDGE ( 'NONE', *, *, #3720, .F. ) ;
#20334=( BOUNDED_CURVE ( )  B_SPLINE_CURVE ( 2, ( #18476, #16550, #12883 ),
 .UNSPECIFIED., .F., .F. ) 
 B_SPLINE_CURVE_WITH_KNOTS ( ( 3, 3 ),
 ( 0.000000000000000000, 0.1752654207116860208 ),
 .UNSPECIFIED. ) 
 CURVE ( )  GEOMETRIC_REPRESENTATION_ITEM ( )  RATIONAL_B_SPLINE_CURVE ( ( 1.000000000000000000, 1.154700538379249908, 1.000000000000000000 ) ) 
 REPRESENTATION_ITEM ( '' )  );
#20406=ORIENTED_EDGE ( 'NONE', *, *, #9828, .T. ) ;
#20478=AXIS2_PLACEMENT_3D ( 'NONE', #8195, #15425, #15676 ) ;
#20479=PLANE ( 'NONE',  #14134 ) ;
#20545=ORIENTED_EDGE ( 'NONE', *, *, #17355, .F. ) ;
#20608=DIRECTION ( 'NONE',  ( -2.056924381537025249E-14, 6.140746379865968924E-31, -1.000000000000000000 ) ) ;
#20609=AXIS2_PLACEMENT_3D ( 'NONE', #17402, #21303, #22721 ) ;
#20694=LINE ( 'NONE', #22579, #13018 ) ;
#20698=ADVANCED_FACE ( 'NONE', ( #27, #12655 ), #151, .T. ) ;
#20738=CIRCLE ( 'NONE', #2154, 2.500000000000000888 ) ;
#20745=DIRECTION ( 'NONE',  ( -0.9730401042858020100, 0.2306359803922089780, -1.063156381331940130E-15 ) ) ;
#20801=VERTEX_POINT ( 'NONE', #18579 ) ;
#20813=CARTESIAN_POINT ( 'NONE',  ( 34.03302451342609913, 9.759458723927547652, 29.25000000000000000 ) ) ;
#20824=DIRECTION ( 'NONE',  ( 6.123230199561429643E-17, 4.868008300101910084E-15, 1.000000000000000000 ) ) ;
#20866=PRODUCT_DEFINITION_FORMATION_WITH_SPECIFIED_SOURCE ( 'ANY', '', #15527, .NOT_KNOWN. ) ;
#20875=CARTESIAN_POINT ( 'NONE',  ( 36.34169561367309598, 12.92845737834490016, 29.25000000000000000 ) ) ;
#20910=DIRECTION ( 'NONE',  ( -0.2306359803922101437, -0.9730401042858017879, 4.316864774682981680E-15 ) ) ;
#20989=ORIENTED_EDGE ( 'NONE', *, *, #14434, .F. ) ;
#21190=CARTESIAN_POINT ( 'NONE',  ( 35.09747506357100377, 11.43410645592859964, 27.68999999999999773 ) ) ;
#21206=ORIENTED_EDGE ( 'NONE', *, *, #10518, .T. ) ;
#21228=ORIENTED_EDGE ( 'NONE', *, *, #11732, .T. ) ;
#21233=( GEOMETRIC_REPRESENTATION_CONTEXT ( 3 ) GLOBAL_UNCERTAINTY_ASSIGNED_CONTEXT ( ( #7525 ) ) GLOBAL_UNIT_ASSIGNED_CONTEXT ( ( #17598, #3567, #23376 ) ) REPRESENTATION_CONTEXT ( 'NONE', 'WORKASPACE' ) );
#21303=DIRECTION ( 'NONE',  ( -6.123230199561449365E-17, -4.868008300101910084E-15, -1.000000000000000000 ) ) ;
#21344=AXIS2_PLACEMENT_3D ( 'NONE', #22732, #4705, #22971 ) ;
#21346=AXIS2_PLACEMENT_3D ( 'NONE', #20875, #4615, #9855 ) ;
#21387=VERTEX_POINT ( 'NONE', #14972 ) ;
#21390=DIRECTION ( 'NONE',  ( 0.2306359803922102825, 0.9730401042858017879, -4.163336342344335449E-15 ) ) ;
#21490=FACE_OUTER_BOUND ( 'NONE', #5176, .T. ) ;
#21508=EDGE_CURVE ( 'NONE', #16644, #989, #13048, .T. ) ;
#21518=CARTESIAN_POINT ( 'NONE',  ( 34.40556712239430226, 8.514986143071229918, 28.46999999999999886 ) ) ;
#21525=DIRECTION ( 'NONE',  ( -6.123230199561459225E-17, -4.868008300101910084E-15, -1.000000000000000000 ) ) ;
#21753=AXIS2_PLACEMENT_3D ( 'NONE', #17366, #16914, #7896 ) ;
#21827=EDGE_CURVE ( 'NONE', #13418, #18259, #18088, .T. ) ;
#21890=VECTOR ( 'NONE', #9145, 1000.000000000000000 ) ;
#22025=CARTESIAN_POINT ( 'NONE',  ( 36.78282996199610722, 11.03463321983590006, 27.68999999999999773 ) ) ;
#22108=EDGE_CURVE ( 'NONE', #14944, #8200, #3025, .T. ) ;
#22120=ORIENTED_EDGE ( 'NONE', *, *, #15900, .F. ) ;
#22126=CARTESIAN_POINT ( 'NONE',  ( 36.05760157943844035, 11.72988078058867245, 10.50000000000019185 ) ) ;
#22183=EDGE_CURVE ( 'NONE', #23121, #12383, #15203, .T. ) ;
#22217=CARTESIAN_POINT ( 'NONE',  ( 35.59419854219520118, 9.774809681453550780, 26.88000000000000256 ) ) ;
#22251=CARTESIAN_POINT ( 'NONE',  ( 35.59419854219520118, 9.774809681453550780, 26.88000000000000256 ) ) ;
#22263=EDGE_CURVE ( 'NONE', #20801, #17589, #16962, .T. ) ;
#22281=EDGE_CURVE ( 'NONE', #989, #3393, #8566, .T. ) ;
#22288=DIRECTION ( 'NONE',  ( -0.2306359803922101437, -0.9730401042858018990, 4.373252460445732608E-15 ) ) ;
#22290=ORIENTED_EDGE ( 'NONE', *, *, #3720, .T. ) ;
#22335=CARTESIAN_POINT ( 'NONE',  ( 30.97225804683764139, 10.87033058831654131, 26.87999999999999545 ) ) ;
#22397=ADVANCED_FACE ( 'NONE', ( #18707 ), #10548, .F. ) ;
#22531=CARTESIAN_POINT ( 'NONE',  ( 35.59419854219520118, 9.774809681453559662, 29.25000000000000000 ) ) ;
#22579=CARTESIAN_POINT ( 'NONE',  ( 36.09092202081949807, 8.115512906978469942, 28.46999999999999886 ) ) ;
#22625=CIRCLE ( 'NONE', #18483, 4.750000000000000000 ) ;
#22721=DIRECTION ( 'NONE',  ( 0.2306359803922084506, 0.9730401042858022320, -5.112869192352694760E-15 ) ) ;
#22732=CARTESIAN_POINT ( 'NONE',  ( 32.96699026062353255, 10.39752682851250398, 26.29999999999999716 ) ) ;
#22802=DIRECTION ( 'NONE',  ( 0.9730401042858020100, -0.2306359803922089780, 0.000000000000000000 ) ) ;
#22858=CARTESIAN_POINT ( 'NONE',  ( 35.94015251278350576, 11.23436983788223209, 27.55602540378454179 ) ) ;
#22949=DIRECTION ( 'NONE',  ( -0.2306359803922088947, -0.9730401042858021210, 5.139921410301650007E-15 ) ) ;
#22971=DIRECTION ( 'NONE',  ( 0.9730401042858026761, -0.2306359803922063967, 0.000000000000000000 ) ) ;
#23043=EDGE_LOOP ( 'NONE', ( #14250, #10109, #1129, #17694, #14931 ) ) ;
#23121=VERTEX_POINT ( 'NONE', #6393 ) ;
#23143=ADVANCED_FACE ( 'NONE', ( #2834 ), #15407, .F. ) ;
#23151=DIRECTION ( 'NONE',  ( -6.123230199561459225E-17, -4.868008300101910084E-15, -1.000000000000000000 ) ) ;
#23220=CARTESIAN_POINT ( 'NONE',  ( 35.24824457160688240, 8.315249525024842825, 27.55602540378454535 ) ) ;
#23253=DIRECTION ( 'NONE',  ( -6.123230199561429643E-17, -4.868008300101910084E-15, -1.000000000000000000 ) ) ;
#23256=CIRCLE ( 'NONE', #21753, 2.500000000000000888 ) ;
#23286=ORIENTED_EDGE ( 'NONE', *, *, #18337, .T. ) ;
#23296=ADVANCED_FACE ( 'NONE', ( #16343 ), #1850, .F. ) ;
#23330=AXIS2_PLACEMENT_3D ( 'NONE', #18144, #20031, #18256 ) ;
#23367=VERTEX_POINT ( 'NONE', #3752 ) ;
#23376=( NAMED_UNIT ( * ) SI_UNIT ( $, .STERADIAN. ) SOLID_ANGLE_UNIT ( ) );
#23417=DIRECTION ( 'NONE',  ( 5.964507377817269296E-17, 4.861311874385510251E-15, 1.000000000000000000 ) ) ;
#23522=COLOUR_RGB('Light Blue', 0.66274510, 0.83137255, 0.94901961);
#23523=FILL_AREA_STYLE_COLOUR('',#23522);
#23524=FILL_AREA_STYLE('',(#23523));
#23525=SURFACE_STYLE_FILL_AREA(#23524);
#23526=SURFACE_SIDE_STYLE('',(#23525));
#23527=SURFACE_STYLE_USAGE(.BOTH.,#23526);
#23528=PRESENTATION_STYLE_ASSIGNMENT((#23527));
#23561=STYLED_ITEM('',(#23528),#16939);
#23562=MECHANICAL_DESIGN_GEOMETRIC_PRESENTATION_REPRESENTATION('',(#23561),#21233);
ENDSEC;
END-ISO-10303-21;
